ISO-10303-21;
HEADER;
/* Generated by software containing ST-Developer
 * from STEP Tools, Inc. (www.steptools.com) 
 */

FILE_DESCRIPTION(
/* description */ ('Cable chain and bracket set'),
/* implementation_level */ '2;1');

FILE_NAME(
/* name */ 'Hex Nut - M6.step',
/* time_stamp */ '2026-10-29T17:19:47-07:00',
/* author */ (''),
/* organization */ (''),
/* preprocessor_version */ 'ST-DEVELOPER v20.2',
/* originating_system */ 'Autodesk Translation Framework v15.17.0.0',
/* authorisation */ '');

FILE_SCHEMA (('AUTOMOTIVE_DESIGN { 1 0 10303 214 3 1 1 }'));
ENDSEC;

DATA;
#10=MECHANICAL_DESIGN_GEOMETRIC_PRESENTATION_REPRESENTATION('',(#349),#5929);
#271=(
BOUNDED_CURVE()
B_SPLINE_CURVE(2,(#5757,#5758,#5759),.UNSPECIFIED.,.F.,.F.)
B_SPLINE_CURVE_WITH_KNOTS((3,3),(0.144988513094728,0.791574906712449),
 .UNSPECIFIED.)
CURVE()
GEOMETRIC_REPRESENTATION_ITEM()
RATIONAL_B_SPLINE_CURVE((1.09282032302755,1.26188021535082,1.09282032302931))
REPRESENTATION_ITEM('')
);
#272=(
BOUNDED_CURVE()
B_SPLINE_CURVE(2,(#5761,#5762,#5763),.UNSPECIFIED.,.F.,.F.)
B_SPLINE_CURVE_WITH_KNOTS((3,3),(0.144988513094728,0.791574906712449),
 .UNSPECIFIED.)
CURVE()
GEOMETRIC_REPRESENTATION_ITEM()
RATIONAL_B_SPLINE_CURVE((1.09282032302755,1.26188021535082,1.09282032302931))
REPRESENTATION_ITEM('')
);
#273=(
BOUNDED_CURVE()
B_SPLINE_CURVE(2,(#5768,#5769,#5770),.UNSPECIFIED.,.F.,.F.)
B_SPLINE_CURVE_WITH_KNOTS((3,3),(0.144988513094728,0.791574906712449),
 .UNSPECIFIED.)
CURVE()
GEOMETRIC_REPRESENTATION_ITEM()
RATIONAL_B_SPLINE_CURVE((1.09282032302755,1.26188021535082,1.09282032302931))
REPRESENTATION_ITEM('')
);
#274=(
BOUNDED_CURVE()
B_SPLINE_CURVE(2,(#5772,#5773,#5774),.UNSPECIFIED.,.F.,.F.)
B_SPLINE_CURVE_WITH_KNOTS((3,3),(0.144988513094728,0.791574906712449),
 .UNSPECIFIED.)
CURVE()
GEOMETRIC_REPRESENTATION_ITEM()
RATIONAL_B_SPLINE_CURVE((1.09282032302755,1.26188021535082,1.09282032302931))
REPRESENTATION_ITEM('')
);
#275=(
BOUNDED_CURVE()
B_SPLINE_CURVE(2,(#5776,#5777,#5778),.UNSPECIFIED.,.F.,.F.)
B_SPLINE_CURVE_WITH_KNOTS((3,3),(0.144988513094728,0.791574906712449),
 .UNSPECIFIED.)
CURVE()
GEOMETRIC_REPRESENTATION_ITEM()
RATIONAL_B_SPLINE_CURVE((1.09282032302755,1.26188021535082,1.09282032302931))
REPRESENTATION_ITEM('')
);
#276=(
BOUNDED_CURVE()
B_SPLINE_CURVE(2,(#5779,#5780,#5781),.UNSPECIFIED.,.F.,.F.)
B_SPLINE_CURVE_WITH_KNOTS((3,3),(0.144988513094728,0.791574906712449),
 .UNSPECIFIED.)
CURVE()
GEOMETRIC_REPRESENTATION_ITEM()
RATIONAL_B_SPLINE_CURVE((1.09282032302755,1.26188021535082,1.09282032302931))
REPRESENTATION_ITEM('')
);
#277=(
BOUNDED_CURVE()
B_SPLINE_CURVE(2,(#5788,#5789,#5790),.UNSPECIFIED.,.F.,.F.)
B_SPLINE_CURVE_WITH_KNOTS((3,3),(0.144988513094728,0.791574906712449),
 .UNSPECIFIED.)
CURVE()
GEOMETRIC_REPRESENTATION_ITEM()
RATIONAL_B_SPLINE_CURVE((1.09282032302755,1.26188021535082,1.09282032302931))
REPRESENTATION_ITEM('')
);
#278=(
BOUNDED_CURVE()
B_SPLINE_CURVE(2,(#5792,#5793,#5794),.UNSPECIFIED.,.F.,.F.)
B_SPLINE_CURVE_WITH_KNOTS((3,3),(0.144988513094727,0.791574906712449),
 .UNSPECIFIED.)
CURVE()
GEOMETRIC_REPRESENTATION_ITEM()
RATIONAL_B_SPLINE_CURVE((1.09282032302755,1.26188021535082,1.09282032302931))
REPRESENTATION_ITEM('')
);
#279=(
BOUNDED_CURVE()
B_SPLINE_CURVE(2,(#5796,#5797,#5798),.UNSPECIFIED.,.F.,.F.)
B_SPLINE_CURVE_WITH_KNOTS((3,3),(0.144988513094728,0.791574906712449),
 .UNSPECIFIED.)
CURVE()
GEOMETRIC_REPRESENTATION_ITEM()
RATIONAL_B_SPLINE_CURVE((1.09282032302755,1.26188021535082,1.09282032302931))
REPRESENTATION_ITEM('')
);
#280=(
BOUNDED_CURVE()
B_SPLINE_CURVE(2,(#5800,#5801,#5802),.UNSPECIFIED.,.F.,.F.)
B_SPLINE_CURVE_WITH_KNOTS((3,3),(0.144988513094728,0.791574906712449),
 .UNSPECIFIED.)
CURVE()
GEOMETRIC_REPRESENTATION_ITEM()
RATIONAL_B_SPLINE_CURVE((1.09282032302755,1.26188021535082,1.09282032302931))
REPRESENTATION_ITEM('')
);
#281=(
BOUNDED_CURVE()
B_SPLINE_CURVE(2,(#5804,#5805,#5806),.UNSPECIFIED.,.F.,.F.)
B_SPLINE_CURVE_WITH_KNOTS((3,3),(0.144988513094728,0.791574906712449),
 .UNSPECIFIED.)
CURVE()
GEOMETRIC_REPRESENTATION_ITEM()
RATIONAL_B_SPLINE_CURVE((1.09282032302755,1.26188021535082,1.09282032302931))
REPRESENTATION_ITEM('')
);
#282=(
BOUNDED_CURVE()
B_SPLINE_CURVE(2,(#5807,#5808,#5809),.UNSPECIFIED.,.F.,.F.)
B_SPLINE_CURVE_WITH_KNOTS((3,3),(0.144988513094727,0.791574906712449),
 .UNSPECIFIED.)
CURVE()
GEOMETRIC_REPRESENTATION_ITEM()
RATIONAL_B_SPLINE_CURVE((1.09282032302755,1.26188021535082,1.09282032302931))
REPRESENTATION_ITEM('')
);
#289=CONICAL_SURFACE('',#3747,0.576175134594813,1.0471975511966);
#290=CONICAL_SURFACE('',#3749,0.576175134594813,1.0471975511966);
#323=SHAPE_REPRESENTATION_RELATIONSHIP('SRR','None',#6061,#336);
#336=ADVANCED_BREP_SHAPE_REPRESENTATION('',(#362),#5928);
#349=STYLED_ITEM('',(#6227),#362);
#362=MANIFOLD_SOLID_BREP('Body1',#3343);
#403=FACE_BOUND('',#930,.T.);
#404=FACE_BOUND('',#932,.T.);
#519=PLANE('',#3751);
#520=PLANE('',#3752);
#521=PLANE('',#3753);
#522=PLANE('',#3757);
#523=PLANE('',#3758);
#524=PLANE('',#3759);
#525=PLANE('',#3760);
#526=PLANE('',#3761);
#698=FACE_OUTER_BOUND('',#920,.T.);
#699=FACE_OUTER_BOUND('',#921,.T.);
#700=FACE_OUTER_BOUND('',#922,.T.);
#701=FACE_OUTER_BOUND('',#923,.T.);
#702=FACE_OUTER_BOUND('',#924,.T.);
#703=FACE_OUTER_BOUND('',#925,.T.);
#704=FACE_OUTER_BOUND('',#926,.T.);
#705=FACE_OUTER_BOUND('',#927,.T.);
#706=FACE_OUTER_BOUND('',#928,.T.);
#707=FACE_OUTER_BOUND('',#929,.T.);
#708=FACE_OUTER_BOUND('',#931,.T.);
#920=EDGE_LOOP('',(#3047,#3048,#3049,#3050,#3051,#3052,#3053,#3054,#3055));
#921=EDGE_LOOP('',(#3056,#3057,#3058,#3059,#3060,#3061,#3062,#3063,#3064));
#922=EDGE_LOOP('',(#3065,#3066,#3067,#3068));
#923=EDGE_LOOP('',(#3069,#3070,#3071,#3072));
#924=EDGE_LOOP('',(#3073,#3074,#3075,#3076));
#925=EDGE_LOOP('',(#3077,#3078,#3079,#3080));
#926=EDGE_LOOP('',(#3081,#3082,#3083,#3084));
#927=EDGE_LOOP('',(#3085,#3086,#3087,#3088));
#928=EDGE_LOOP('',(#3089,#3090,#3091,#3092));
#929=EDGE_LOOP('',(#3093));
#930=EDGE_LOOP('',(#3094));
#931=EDGE_LOOP('',(#3095));
#932=EDGE_LOOP('',(#3096));
#1184=LINE('',#5765,#1444);
#1185=LINE('',#5786,#1445);
#1186=LINE('',#5811,#1446);
#1187=LINE('',#5812,#1447);
#1188=LINE('',#5814,#1448);
#1189=LINE('',#5816,#1449);
#1190=LINE('',#5821,#1450);
#1191=LINE('',#5824,#1451);
#1192=LINE('',#5826,#1452);
#1444=VECTOR('',#4717,0.576175134594813);
#1445=VECTOR('',#4724,0.576175134594813);
#1446=VECTOR('',#4727,1.);
#1447=VECTOR('',#4728,1.);
#1448=VECTOR('',#4731,1.);
#1449=VECTOR('',#4734,1.);
#1450=VECTOR('',#4739,0.3);
#1451=VECTOR('',#4744,1.);
#1452=VECTOR('',#4747,1.);
#1557=CIRCLE('',#3748,0.475);
#1558=CIRCLE('',#3750,0.475);
#1559=CIRCLE('',#3755,0.25175);
#1560=CIRCLE('',#3756,0.25175);
#1809=VERTEX_POINT('',#5755);
#1810=VERTEX_POINT('',#5756);
#1811=VERTEX_POINT('',#5760);
#1812=VERTEX_POINT('',#5764);
#1813=VERTEX_POINT('',#5767);
#1814=VERTEX_POINT('',#5771);
#1815=VERTEX_POINT('',#5775);
#1816=VERTEX_POINT('',#5783);
#1817=VERTEX_POINT('',#5785);
#1818=VERTEX_POINT('',#5787);
#1819=VERTEX_POINT('',#5791);
#1820=VERTEX_POINT('',#5795);
#1821=VERTEX_POINT('',#5799);
#1822=VERTEX_POINT('',#5803);
#1823=VERTEX_POINT('',#5818);
#1824=VERTEX_POINT('',#5820);
#2224=EDGE_CURVE('',#1809,#1810,#271,.T.);
#2225=EDGE_CURVE('',#1811,#1809,#272,.T.);
#2226=EDGE_CURVE('',#1811,#1812,#1184,.T.);
#2227=EDGE_CURVE('',#1812,#1812,#1557,.T.);
#2228=EDGE_CURVE('',#1813,#1811,#273,.T.);
#2229=EDGE_CURVE('',#1814,#1813,#274,.T.);
#2230=EDGE_CURVE('',#1815,#1814,#275,.T.);
#2231=EDGE_CURVE('',#1810,#1815,#276,.T.);
#2232=EDGE_CURVE('',#1816,#1816,#1558,.T.);
#2233=EDGE_CURVE('',#1816,#1817,#1185,.T.);
#2234=EDGE_CURVE('',#1818,#1817,#277,.T.);
#2235=EDGE_CURVE('',#1819,#1818,#278,.T.);
#2236=EDGE_CURVE('',#1820,#1819,#279,.T.);
#2237=EDGE_CURVE('',#1821,#1820,#280,.T.);
#2238=EDGE_CURVE('',#1822,#1821,#281,.T.);
#2239=EDGE_CURVE('',#1817,#1822,#282,.T.);
#2240=EDGE_CURVE('',#1813,#1822,#1186,.T.);
#2241=EDGE_CURVE('',#1814,#1821,#1187,.T.);
#2242=EDGE_CURVE('',#1811,#1817,#1188,.T.);
#2243=EDGE_CURVE('',#1809,#1818,#1189,.T.);
#2244=EDGE_CURVE('',#1823,#1823,#1559,.F.);
#2245=EDGE_CURVE('',#1823,#1824,#1190,.T.);
#2246=EDGE_CURVE('',#1824,#1824,#1560,.F.);
#2247=EDGE_CURVE('',#1810,#1819,#1191,.T.);
#2248=EDGE_CURVE('',#1815,#1820,#1192,.T.);
#3047=ORIENTED_EDGE('',*,*,#2224,.F.);
#3048=ORIENTED_EDGE('',*,*,#2225,.F.);
#3049=ORIENTED_EDGE('',*,*,#2226,.T.);
#3050=ORIENTED_EDGE('',*,*,#2227,.F.);
#3051=ORIENTED_EDGE('',*,*,#2226,.F.);
#3052=ORIENTED_EDGE('',*,*,#2228,.F.);
#3053=ORIENTED_EDGE('',*,*,#2229,.F.);
#3054=ORIENTED_EDGE('',*,*,#2230,.F.);
#3055=ORIENTED_EDGE('',*,*,#2231,.F.);
#3056=ORIENTED_EDGE('',*,*,#2232,.F.);
#3057=ORIENTED_EDGE('',*,*,#2233,.T.);
#3058=ORIENTED_EDGE('',*,*,#2234,.F.);
#3059=ORIENTED_EDGE('',*,*,#2235,.F.);
#3060=ORIENTED_EDGE('',*,*,#2236,.F.);
#3061=ORIENTED_EDGE('',*,*,#2237,.F.);
#3062=ORIENTED_EDGE('',*,*,#2238,.F.);
#3063=ORIENTED_EDGE('',*,*,#2239,.F.);
#3064=ORIENTED_EDGE('',*,*,#2233,.F.);
#3065=ORIENTED_EDGE('',*,*,#2229,.T.);
#3066=ORIENTED_EDGE('',*,*,#2240,.T.);
#3067=ORIENTED_EDGE('',*,*,#2238,.T.);
#3068=ORIENTED_EDGE('',*,*,#2241,.F.);
#3069=ORIENTED_EDGE('',*,*,#2228,.T.);
#3070=ORIENTED_EDGE('',*,*,#2242,.T.);
#3071=ORIENTED_EDGE('',*,*,#2239,.T.);
#3072=ORIENTED_EDGE('',*,*,#2240,.F.);
#3073=ORIENTED_EDGE('',*,*,#2225,.T.);
#3074=ORIENTED_EDGE('',*,*,#2243,.T.);
#3075=ORIENTED_EDGE('',*,*,#2234,.T.);
#3076=ORIENTED_EDGE('',*,*,#2242,.F.);
#3077=ORIENTED_EDGE('',*,*,#2244,.F.);
#3078=ORIENTED_EDGE('',*,*,#2245,.T.);
#3079=ORIENTED_EDGE('',*,*,#2246,.T.);
#3080=ORIENTED_EDGE('',*,*,#2245,.F.);
#3081=ORIENTED_EDGE('',*,*,#2224,.T.);
#3082=ORIENTED_EDGE('',*,*,#2247,.T.);
#3083=ORIENTED_EDGE('',*,*,#2235,.T.);
#3084=ORIENTED_EDGE('',*,*,#2243,.F.);
#3085=ORIENTED_EDGE('',*,*,#2230,.T.);
#3086=ORIENTED_EDGE('',*,*,#2241,.T.);
#3087=ORIENTED_EDGE('',*,*,#2237,.T.);
#3088=ORIENTED_EDGE('',*,*,#2248,.F.);
#3089=ORIENTED_EDGE('',*,*,#2231,.T.);
#3090=ORIENTED_EDGE('',*,*,#2248,.T.);
#3091=ORIENTED_EDGE('',*,*,#2236,.T.);
#3092=ORIENTED_EDGE('',*,*,#2247,.F.);
#3093=ORIENTED_EDGE('',*,*,#2232,.T.);
#3094=ORIENTED_EDGE('',*,*,#2244,.T.);
#3095=ORIENTED_EDGE('',*,*,#2227,.T.);
#3096=ORIENTED_EDGE('',*,*,#2246,.F.);
#3148=CYLINDRICAL_SURFACE('',#3754,0.25175);
#3320=ADVANCED_FACE('',(#698),#289,.T.);
#3321=ADVANCED_FACE('',(#699),#290,.T.);
#3322=ADVANCED_FACE('',(#700),#519,.T.);
#3323=ADVANCED_FACE('',(#701),#520,.T.);
#3324=ADVANCED_FACE('',(#702),#521,.T.);
#3325=ADVANCED_FACE('',(#703),#3148,.F.);
#3326=ADVANCED_FACE('',(#704),#522,.T.);
#3327=ADVANCED_FACE('',(#705),#523,.T.);
#3328=ADVANCED_FACE('',(#706),#524,.T.);
#3329=ADVANCED_FACE('',(#707,#403),#525,.T.);
#3330=ADVANCED_FACE('',(#708,#404),#526,.F.);
#3343=CLOSED_SHELL('',(#3320,#3321,#3322,#3323,#3324,#3325,#3326,#3327,
#3328,#3329,#3330));
#3746=AXIS2_PLACEMENT_3D('',#5753,#4713,#4714);
#3747=AXIS2_PLACEMENT_3D('',#5754,#4715,#4716);
#3748=AXIS2_PLACEMENT_3D('',#5766,#4718,#4719);
#3749=AXIS2_PLACEMENT_3D('',#5782,#4720,#4721);
#3750=AXIS2_PLACEMENT_3D('',#5784,#4722,#4723);
#3751=AXIS2_PLACEMENT_3D('',#5810,#4725,#4726);
#3752=AXIS2_PLACEMENT_3D('',#5813,#4729,#4730);
#3753=AXIS2_PLACEMENT_3D('',#5815,#4732,#4733);
#3754=AXIS2_PLACEMENT_3D('',#5817,#4735,#4736);
#3755=AXIS2_PLACEMENT_3D('',#5819,#4737,#4738);
#3756=AXIS2_PLACEMENT_3D('',#5822,#4740,#4741);
#3757=AXIS2_PLACEMENT_3D('',#5823,#4742,#4743);
#3758=AXIS2_PLACEMENT_3D('',#5825,#4745,#4746);
#3759=AXIS2_PLACEMENT_3D('',#5827,#4748,#4749);
#3760=AXIS2_PLACEMENT_3D('',#5828,#4750,#4751);
#3761=AXIS2_PLACEMENT_3D('',#5829,#4752,#4753);
#4713=DIRECTION('axis',(0.,0.,1.));
#4714=DIRECTION('refdir',(1.,0.,0.));
#4715=DIRECTION('center_axis',(0.,1.,0.));
#4716=DIRECTION('ref_axis',(1.,0.,0.));
#4717=DIRECTION('',(0.866025403784439,-0.5,1.06057523872491E-16));
#4718=DIRECTION('center_axis',(0.,-1.,0.));
#4719=DIRECTION('ref_axis',(1.,0.,0.));
#4720=DIRECTION('center_axis',(0.,-1.,0.));
#4721=DIRECTION('ref_axis',(1.,0.,0.));
#4722=DIRECTION('center_axis',(0.,1.,0.));
#4723=DIRECTION('ref_axis',(1.,0.,0.));
#4724=DIRECTION('',(-0.866025403784439,-0.5,-1.06057523872491E-16));
#4725=DIRECTION('center_axis',(1.92296268638356E-16,0.,-1.));
#4726=DIRECTION('ref_axis',(-1.,0.,-1.92296268638356E-16));
#4727=DIRECTION('',(0.,1.,0.));
#4728=DIRECTION('',(0.,1.,0.));
#4729=DIRECTION('center_axis',(-0.866025403784439,0.,-0.5));
#4730=DIRECTION('ref_axis',(-0.5,0.,0.866025403784439));
#4731=DIRECTION('',(0.,1.,0.));
#4732=DIRECTION('center_axis',(-0.866025403784439,0.,0.5));
#4733=DIRECTION('ref_axis',(0.5,0.,0.866025403784439));
#4734=DIRECTION('',(0.,1.,0.));
#4735=DIRECTION('center_axis',(0.,1.,0.));
#4736=DIRECTION('ref_axis',(1.,0.,0.));
#4737=DIRECTION('center_axis',(0.,1.,0.));
#4738=DIRECTION('ref_axis',(1.,0.,0.));
#4739=DIRECTION('',(0.,-1.,0.));
#4740=DIRECTION('center_axis',(0.,1.,0.));
#4741=DIRECTION('ref_axis',(1.,0.,0.));
#4742=DIRECTION('center_axis',(-1.92296268638356E-16,0.,1.));
#4743=DIRECTION('ref_axis',(1.,0.,1.92296268638356E-16));
#4744=DIRECTION('',(0.,1.,0.));
#4745=DIRECTION('center_axis',(0.866025403784439,0.,-0.5));
#4746=DIRECTION('ref_axis',(-0.5,0.,-0.866025403784439));
#4747=DIRECTION('',(0.,1.,0.));
#4748=DIRECTION('center_axis',(0.866025403784439,0.,0.5));
#4749=DIRECTION('ref_axis',(0.5,0.,-0.866025403784439));
#4750=DIRECTION('center_axis',(0.,1.,0.));
#4751=DIRECTION('ref_axis',(1.,0.,0.));
#4752=DIRECTION('center_axis',(0.,1.,0.));
#4753=DIRECTION('ref_axis',(1.,0.,0.));
#5753=CARTESIAN_POINT('',(0.,0.,0.));
#5754=CARTESIAN_POINT('Origin',(0.,0.0584134911936118,0.));
#5755=CARTESIAN_POINT('',(-0.288675134594813,0.0590919554682611,0.5));
#5756=CARTESIAN_POINT('',(0.288675134594813,0.0590919554682611,0.5));
#5757=CARTESIAN_POINT('Ctrl Pts',(-0.288675134594813,0.0590919554682611,
0.5));
#5758=CARTESIAN_POINT('Ctrl Pts',(2.1664336991023E-12,-0.0242413778636964,
0.5));
#5759=CARTESIAN_POINT('Ctrl Pts',(0.288675134594813,0.0590919554682611,
0.5));
#5760=CARTESIAN_POINT('',(-0.577350269189626,0.0590919554682611,-7.07050159149938E-17));
#5761=CARTESIAN_POINT('Ctrl Pts',(-0.577350269189626,0.0590919554682611,
-7.07050159149938E-17));
#5762=CARTESIAN_POINT('Ctrl Pts',(-0.433012701891136,-0.0242413778636963,
0.250000000001876));
#5763=CARTESIAN_POINT('Ctrl Pts',(-0.288675134594813,0.0590919554682611,
0.5));
#5764=CARTESIAN_POINT('',(-0.475,-4.16333634234434E-17,-5.81707229594993E-17));
#5765=CARTESIAN_POINT('',(-0.576175134594813,0.0584134911936118,-7.05611034329833E-17));
#5766=CARTESIAN_POINT('Origin',(0.,0.,0.));
#5767=CARTESIAN_POINT('',(-0.288675134594813,0.0590919554682611,-0.5));
#5768=CARTESIAN_POINT('Ctrl Pts',(-0.288675134594813,0.0590919554682611,
-0.5));
#5769=CARTESIAN_POINT('Ctrl Pts',(-0.433012701893303,-0.0242413778636963,
-0.249999999998124));
#5770=CARTESIAN_POINT('Ctrl Pts',(-0.577350269189626,0.0590919554682611,
-7.07050159149938E-17));
#5771=CARTESIAN_POINT('',(0.288675134594813,0.0590919554682611,-0.5));
#5772=CARTESIAN_POINT('Ctrl Pts',(0.288675134594813,0.0590919554682611,
-0.5));
#5773=CARTESIAN_POINT('Ctrl Pts',(-2.16648921025353E-12,-0.0242413778636962,
-0.5));
#5774=CARTESIAN_POINT('Ctrl Pts',(-0.288675134594813,0.0590919554682611,
-0.5));
#5775=CARTESIAN_POINT('',(0.577350269189626,0.0590919554682611,0.));
#5776=CARTESIAN_POINT('Ctrl Pts',(0.577350269189626,0.0590919554682611,
0.));
#5777=CARTESIAN_POINT('Ctrl Pts',(0.433012701891136,-0.0242413778636963,
-0.250000000001876));
#5778=CARTESIAN_POINT('Ctrl Pts',(0.288675134594813,0.0590919554682611,
-0.5));
#5779=CARTESIAN_POINT('Ctrl Pts',(0.288675134594813,0.0590919554682611,
0.5));
#5780=CARTESIAN_POINT('Ctrl Pts',(0.433012701893303,-0.0242413778636962,
0.249999999998124));
#5781=CARTESIAN_POINT('Ctrl Pts',(0.577350269189626,0.0590919554682611,
0.));
#5782=CARTESIAN_POINT('Origin',(0.,0.461586508806388,0.));
#5783=CARTESIAN_POINT('',(-0.475,0.52,-5.81707229594993E-17));
#5784=CARTESIAN_POINT('Origin',(0.,0.52,0.));
#5785=CARTESIAN_POINT('',(-0.577350269189626,0.460908044531739,-7.07050159149938E-17));
#5786=CARTESIAN_POINT('',(-0.576175134594813,0.461586508806388,-7.05611034329833E-17));
#5787=CARTESIAN_POINT('',(-0.288675134594813,0.460908044531739,0.5));
#5788=CARTESIAN_POINT('Ctrl Pts',(-0.288675134594813,0.460908044531739,
0.5));
#5789=CARTESIAN_POINT('Ctrl Pts',(-0.433012701893303,0.544241377863696,
0.249999999998124));
#5790=CARTESIAN_POINT('Ctrl Pts',(-0.577350269189626,0.460908044531739,
-7.07050159149938E-17));
#5791=CARTESIAN_POINT('',(0.288675134594813,0.460908044531739,0.5));
#5792=CARTESIAN_POINT('Ctrl Pts',(0.288675134594813,0.460908044531739,0.5));
#5793=CARTESIAN_POINT('Ctrl Pts',(-2.16676676600969E-12,0.544241377863697,
0.5));
#5794=CARTESIAN_POINT('Ctrl Pts',(-0.288675134594813,0.460908044531739,
0.5));
#5795=CARTESIAN_POINT('',(0.577350269189626,0.460908044531739,0.));
#5796=CARTESIAN_POINT('Ctrl Pts',(0.577350269189626,0.460908044531739,0.));
#5797=CARTESIAN_POINT('Ctrl Pts',(0.433012701891136,0.544241377863696,0.250000000001876));
#5798=CARTESIAN_POINT('Ctrl Pts',(0.288675134594813,0.460908044531739,0.5));
#5799=CARTESIAN_POINT('',(0.288675134594813,0.460908044531739,-0.5));
#5800=CARTESIAN_POINT('Ctrl Pts',(0.288675134594813,0.460908044531739,-0.5));
#5801=CARTESIAN_POINT('Ctrl Pts',(0.433012701893302,0.544241377863696,-0.249999999998124));
#5802=CARTESIAN_POINT('Ctrl Pts',(0.577350269189626,0.460908044531739,0.));
#5803=CARTESIAN_POINT('',(-0.288675134594813,0.460908044531739,-0.5));
#5804=CARTESIAN_POINT('Ctrl Pts',(-0.288675134594813,0.460908044531739,
-0.5));
#5805=CARTESIAN_POINT('Ctrl Pts',(2.16660023255599E-12,0.544241377863697,
-0.5));
#5806=CARTESIAN_POINT('Ctrl Pts',(0.288675134594813,0.460908044531739,-0.5));
#5807=CARTESIAN_POINT('Ctrl Pts',(-0.577350269189626,0.460908044531739,
-7.07050159149938E-17));
#5808=CARTESIAN_POINT('Ctrl Pts',(-0.433012701891136,0.544241377863696,
-0.250000000001876));
#5809=CARTESIAN_POINT('Ctrl Pts',(-0.288675134594813,0.460908044531739,
-0.5));
#5810=CARTESIAN_POINT('Origin',(0.288675134594813,0.,-0.5));
#5811=CARTESIAN_POINT('',(-0.288675134594813,0.,-0.5));
#5812=CARTESIAN_POINT('',(0.288675134594813,0.,-0.5));
#5813=CARTESIAN_POINT('Origin',(-0.288675134594813,0.,-0.5));
#5814=CARTESIAN_POINT('',(-0.577350269189626,0.,-7.07050159149938E-17));
#5815=CARTESIAN_POINT('Origin',(-0.577350269189626,0.,-7.07050159149938E-17));
#5816=CARTESIAN_POINT('',(-0.288675134594813,0.,0.5));
#5817=CARTESIAN_POINT('Origin',(0.,0.,0.));
#5818=CARTESIAN_POINT('',(-0.25175,0.52,3.08304831685346E-17));
#5819=CARTESIAN_POINT('Origin',(0.,0.52,0.));
#5820=CARTESIAN_POINT('',(-0.25175,0.,3.08304831685346E-17));
#5821=CARTESIAN_POINT('',(-0.25175,0.,3.08304831685346E-17));
#5822=CARTESIAN_POINT('Origin',(0.,0.,0.));
#5823=CARTESIAN_POINT('Origin',(-0.288675134594813,0.,0.5));
#5824=CARTESIAN_POINT('',(0.288675134594813,0.,0.5));
#5825=CARTESIAN_POINT('Origin',(0.577350269189626,0.,0.));
#5826=CARTESIAN_POINT('',(0.577350269189626,0.,0.));
#5827=CARTESIAN_POINT('Origin',(0.288675134594813,0.,0.5));
#5828=CARTESIAN_POINT('Origin',(0.,0.52,0.));
#5829=CARTESIAN_POINT('Origin',(0.,0.,0.));
#5904=UNCERTAINTY_MEASURE_WITH_UNIT(LENGTH_MEASURE(0.001),#5930,
'DISTANCE_ACCURACY_VALUE',
'Maximum model space distance between geometric entities at asserted c
onnectivities');
#5905=UNCERTAINTY_MEASURE_WITH_UNIT(LENGTH_MEASURE(0.001),#5930,
'DISTANCE_ACCURACY_VALUE',
'Maximum model space distance between geometric entities at asserted c
onnectivities');
#5928=(
GEOMETRIC_REPRESENTATION_CONTEXT(3)
GLOBAL_UNCERTAINTY_ASSIGNED_CONTEXT((#5904))
GLOBAL_UNIT_ASSIGNED_CONTEXT((#5930,#5932,#5933))
REPRESENTATION_CONTEXT('','3D')
);
#5929=(
GEOMETRIC_REPRESENTATION_CONTEXT(3)
GLOBAL_UNCERTAINTY_ASSIGNED_CONTEXT((#5905))
GLOBAL_UNIT_ASSIGNED_CONTEXT((#5930,#5932,#5933))
REPRESENTATION_CONTEXT('','3D')
);
#5930=(
LENGTH_UNIT()
NAMED_UNIT(*)
SI_UNIT(.CENTI.,.METRE.)
);
#5932=(
NAMED_UNIT(*)
PLANE_ANGLE_UNIT()
SI_UNIT($,.RADIAN.)
);
#5933=(
NAMED_UNIT(*)
SI_UNIT($,.STERADIAN.)
SOLID_ANGLE_UNIT()
);
#5956=SHAPE_DEFINITION_REPRESENTATION(#5986,#6061);
#5986=PRODUCT_DEFINITION_SHAPE('',$,#6085);
#6061=SHAPE_REPRESENTATION('',(#3746),#5928);
#6062=PRODUCT_DEFINITION_CONTEXT('part definition',#6133,'design');
#6085=PRODUCT_DEFINITION('Hex Nut - M6','Hex Nut - M6',#6108,#6062);
#6108=PRODUCT_DEFINITION_FORMATION('',$,#6157);
#6133=APPLICATION_CONTEXT(
'Core Data for Automotive Mechanical Design Process');
#6134=PRODUCT_CONTEXT('part definition',#6133,'mechanical');
#6157=PRODUCT('Hex Nut - M6','Hex Nut - M6','Hex Nut - M6',(#6134));
#6221=COLOUR_RGB('Black',0.12,0.14,0.17);
#6222=FILL_AREA_STYLE_COLOUR('',#6221);
#6223=FILL_AREA_STYLE('',(#6222));
#6224=SURFACE_STYLE_FILL_AREA(#6223);
#6225=SURFACE_SIDE_STYLE('',(#6224));
#6226=SURFACE_STYLE_USAGE(.BOTH.,#6225);
#6227=PRESENTATION_STYLE_ASSIGNMENT((#6226));
ENDSEC;
END-ISO-10303-21;
